ISO-10303-21;
HEADER;
/* Generated by software containing ST-Developer
 * from STEP Tools, Inc. (www.steptools.com) 
 */

FILE_DESCRIPTION(
/* description */ ('Double-row support with tensioned shaft'),
/* implementation_level */ '2;1');

FILE_NAME(
/* name */ 'M5x17 screw.step',
/* time_stamp */ '2026-10-27T10:50:35-07:00',
/* author */ (''),
/* organization */ (''),
/* preprocessor_version */ 'ST-DEVELOPER v20.2',
/* originating_system */ 'Autodesk Translation Framework v15.17.0.0',
/* authorisation */ '');

FILE_SCHEMA (('AUTOMOTIVE_DESIGN { 1 0 10303 214 3 1 1 }'));
ENDSEC;

DATA;
#10=MECHANICAL_DESIGN_GEOMETRIC_PRESENTATION_REPRESENTATION('',(#496),#11559);
#393=CONICAL_SURFACE('',#7002,0.4,0.785398163397448);
#394=CONICAL_SURFACE('',#7006,0.41,0.785398163397448);
#395=CONICAL_SURFACE('',#7010,0.26,0.463647609000806);
#407=ORIENTED_CLOSED_SHELL('',*,#6341,.F.);
#410=BREP_WITH_VOIDS('Body1',#6342,(#407));
#432=SHAPE_REPRESENTATION_RELATIONSHIP('SRR','None',#11740,#464);
#464=ADVANCED_BREP_SHAPE_REPRESENTATION('',(#410),#11542);
#496=STYLED_ITEM('',(#11974),#410);
#613=FACE_BOUND('',#1511,.T.);
#800=PLANE('',#6990);
#801=PLANE('',#6991);
#802=PLANE('',#6992);
#803=PLANE('',#6993);
#804=PLANE('',#6994);
#805=PLANE('',#6995);
#806=PLANE('',#6996);
#807=PLANE('',#6997);
#808=PLANE('',#6998);
#809=PLANE('',#7000);
#810=PLANE('',#7008);
#1082=FACE_OUTER_BOUND('',#1497,.T.);
#1083=FACE_OUTER_BOUND('',#1498,.T.);
#1084=FACE_OUTER_BOUND('',#1499,.T.);
#1085=FACE_OUTER_BOUND('',#1500,.T.);
#1086=FACE_OUTER_BOUND('',#1501,.T.);
#1087=FACE_OUTER_BOUND('',#1502,.T.);
#1088=FACE_OUTER_BOUND('',#1503,.T.);
#1089=FACE_OUTER_BOUND('',#1504,.T.);
#1090=FACE_OUTER_BOUND('',#1505,.T.);
#1091=FACE_OUTER_BOUND('',#1506,.T.);
#1092=FACE_OUTER_BOUND('',#1507,.T.);
#1093=FACE_OUTER_BOUND('',#1508,.T.);
#1094=FACE_OUTER_BOUND('',#1509,.T.);
#1095=FACE_OUTER_BOUND('',#1510,.T.);
#1096=FACE_OUTER_BOUND('',#1512,.T.);
#1097=FACE_OUTER_BOUND('',#1513,.T.);
#1497=EDGE_LOOP('',(#5122,#5123,#5124,#5125));
#1498=EDGE_LOOP('',(#5126,#5127,#5128,#5129));
#1499=EDGE_LOOP('',(#5130,#5131,#5132,#5133));
#1500=EDGE_LOOP('',(#5134,#5135,#5136,#5137));
#1501=EDGE_LOOP('',(#5138,#5139,#5140,#5141));
#1502=EDGE_LOOP('',(#5142,#5143,#5144,#5145));
#1503=EDGE_LOOP('',(#5146,#5147,#5148,#5149,#5150,#5151));
#1504=EDGE_LOOP('',(#5152,#5153,#5154,#5155,#5156,#5157));
#1505=EDGE_LOOP('',(#5158));
#1506=EDGE_LOOP('',(#5159));
#1507=EDGE_LOOP('',(#5160,#5161,#5162,#5163));
#1508=EDGE_LOOP('',(#5164,#5165,#5166,#5167));
#1509=EDGE_LOOP('',(#5168,#5169,#5170,#5171));
#1510=EDGE_LOOP('',(#5172));
#1511=EDGE_LOOP('',(#5173));
#1512=EDGE_LOOP('',(#5174,#5175,#5176,#5177));
#1513=EDGE_LOOP('',(#5178,#5179,#5180,#5181));
#2046=LINE('',#10082,#2593);
#2047=LINE('',#10084,#2594);
#2048=LINE('',#10086,#2595);
#2049=LINE('',#10087,#2596);
#2050=LINE('',#10090,#2597);
#2051=LINE('',#10092,#2598);
#2052=LINE('',#10093,#2599);
#2053=LINE('',#10096,#2600);
#2054=LINE('',#10098,#2601);
#2055=LINE('',#10099,#2602);
#2056=LINE('',#10102,#2603);
#2057=LINE('',#10104,#2604);
#2058=LINE('',#10105,#2605);
#2059=LINE('',#10108,#2606);
#2060=LINE('',#10110,#2607);
#2061=LINE('',#10111,#2608);
#2062=LINE('',#10113,#2609);
#2063=LINE('',#10114,#2610);
#2064=LINE('',#10126,#2611);
#2065=LINE('',#10130,#2612);
#2066=LINE('',#10134,#2613);
#2067=LINE('',#10141,#2614);
#2068=LINE('',#10143,#2615);
#2593=VECTOR('',#8231,1.);
#2594=VECTOR('',#8232,1.);
#2595=VECTOR('',#8233,1.);
#2596=VECTOR('',#8234,1.);
#2597=VECTOR('',#8237,1.);
#2598=VECTOR('',#8238,1.);
#2599=VECTOR('',#8239,1.);
#2600=VECTOR('',#8242,1.);
#2601=VECTOR('',#8243,1.);
#2602=VECTOR('',#8244,1.);
#2603=VECTOR('',#8247,1.);
#2604=VECTOR('',#8248,1.);
#2605=VECTOR('',#8249,1.);
#2606=VECTOR('',#8252,1.);
#2607=VECTOR('',#8253,1.);
#2608=VECTOR('',#8254,1.);
#2609=VECTOR('',#8257,1.);
#2610=VECTOR('',#8258,1.);
#2611=VECTOR('',#8275,0.4);
#2612=VECTOR('',#8280,0.425);
#2613=VECTOR('',#8285,0.41);
#2614=VECTOR('',#8294,0.26);
#2615=VECTOR('',#8297,0.25);
#2926=CIRCLE('',#6999,0.24505);
#2927=CIRCLE('',#7001,0.375);
#2928=CIRCLE('',#7003,0.425);
#2929=CIRCLE('',#7005,0.425);
#2930=CIRCLE('',#7007,0.395);
#2931=CIRCLE('',#7009,0.27);
#2932=CIRCLE('',#7011,0.24505);
#3291=VERTEX_POINT('',#10080);
#3292=VERTEX_POINT('',#10081);
#3293=VERTEX_POINT('',#10083);
#3294=VERTEX_POINT('',#10085);
#3295=VERTEX_POINT('',#10089);
#3296=VERTEX_POINT('',#10091);
#3297=VERTEX_POINT('',#10095);
#3298=VERTEX_POINT('',#10097);
#3299=VERTEX_POINT('',#10101);
#3300=VERTEX_POINT('',#10103);
#3301=VERTEX_POINT('',#10107);
#3302=VERTEX_POINT('',#10109);
#3303=VERTEX_POINT('',#10118);
#3304=VERTEX_POINT('',#10121);
#3305=VERTEX_POINT('',#10124);
#3306=VERTEX_POINT('',#10128);
#3307=VERTEX_POINT('',#10132);
#3308=VERTEX_POINT('',#10136);
#3309=VERTEX_POINT('',#10139);
#3946=EDGE_CURVE('',#3291,#3292,#2046,.T.);
#3947=EDGE_CURVE('',#3292,#3293,#2047,.T.);
#3948=EDGE_CURVE('',#3293,#3294,#2048,.T.);
#3949=EDGE_CURVE('',#3291,#3294,#2049,.T.);
#3950=EDGE_CURVE('',#3292,#3295,#2050,.T.);
#3951=EDGE_CURVE('',#3295,#3296,#2051,.T.);
#3952=EDGE_CURVE('',#3296,#3293,#2052,.T.);
#3953=EDGE_CURVE('',#3295,#3297,#2053,.T.);
#3954=EDGE_CURVE('',#3297,#3298,#2054,.T.);
#3955=EDGE_CURVE('',#3298,#3296,#2055,.T.);
#3956=EDGE_CURVE('',#3297,#3299,#2056,.T.);
#3957=EDGE_CURVE('',#3299,#3300,#2057,.T.);
#3958=EDGE_CURVE('',#3300,#3298,#2058,.T.);
#3959=EDGE_CURVE('',#3299,#3301,#2059,.T.);
#3960=EDGE_CURVE('',#3301,#3302,#2060,.T.);
#3961=EDGE_CURVE('',#3302,#3300,#2061,.T.);
#3962=EDGE_CURVE('',#3301,#3291,#2062,.T.);
#3963=EDGE_CURVE('',#3294,#3302,#2063,.T.);
#3964=EDGE_CURVE('',#3303,#3303,#2926,.T.);
#3965=EDGE_CURVE('',#3304,#3304,#2927,.T.);
#3966=EDGE_CURVE('',#3305,#3305,#2928,.T.);
#3967=EDGE_CURVE('',#3305,#3304,#2064,.T.);
#3968=EDGE_CURVE('',#3306,#3306,#2929,.T.);
#3969=EDGE_CURVE('',#3306,#3305,#2065,.T.);
#3970=EDGE_CURVE('',#3307,#3307,#2930,.T.);
#3971=EDGE_CURVE('',#3307,#3306,#2066,.T.);
#3972=EDGE_CURVE('',#3308,#3308,#2931,.T.);
#3973=EDGE_CURVE('',#3309,#3309,#2932,.F.);
#3974=EDGE_CURVE('',#3309,#3308,#2067,.T.);
#3975=EDGE_CURVE('',#3303,#3309,#2068,.T.);
#5122=ORIENTED_EDGE('',*,*,#3946,.T.);
#5123=ORIENTED_EDGE('',*,*,#3947,.T.);
#5124=ORIENTED_EDGE('',*,*,#3948,.T.);
#5125=ORIENTED_EDGE('',*,*,#3949,.F.);
#5126=ORIENTED_EDGE('',*,*,#3950,.T.);
#5127=ORIENTED_EDGE('',*,*,#3951,.T.);
#5128=ORIENTED_EDGE('',*,*,#3952,.T.);
#5129=ORIENTED_EDGE('',*,*,#3947,.F.);
#5130=ORIENTED_EDGE('',*,*,#3953,.T.);
#5131=ORIENTED_EDGE('',*,*,#3954,.T.);
#5132=ORIENTED_EDGE('',*,*,#3955,.T.);
#5133=ORIENTED_EDGE('',*,*,#3951,.F.);
#5134=ORIENTED_EDGE('',*,*,#3956,.T.);
#5135=ORIENTED_EDGE('',*,*,#3957,.T.);
#5136=ORIENTED_EDGE('',*,*,#3958,.T.);
#5137=ORIENTED_EDGE('',*,*,#3954,.F.);
#5138=ORIENTED_EDGE('',*,*,#3959,.T.);
#5139=ORIENTED_EDGE('',*,*,#3960,.T.);
#5140=ORIENTED_EDGE('',*,*,#3961,.T.);
#5141=ORIENTED_EDGE('',*,*,#3957,.F.);
#5142=ORIENTED_EDGE('',*,*,#3962,.T.);
#5143=ORIENTED_EDGE('',*,*,#3949,.T.);
#5144=ORIENTED_EDGE('',*,*,#3963,.T.);
#5145=ORIENTED_EDGE('',*,*,#3960,.F.);
#5146=ORIENTED_EDGE('',*,*,#3962,.F.);
#5147=ORIENTED_EDGE('',*,*,#3959,.F.);
#5148=ORIENTED_EDGE('',*,*,#3956,.F.);
#5149=ORIENTED_EDGE('',*,*,#3953,.F.);
#5150=ORIENTED_EDGE('',*,*,#3950,.F.);
#5151=ORIENTED_EDGE('',*,*,#3946,.F.);
#5152=ORIENTED_EDGE('',*,*,#3963,.F.);
#5153=ORIENTED_EDGE('',*,*,#3948,.F.);
#5154=ORIENTED_EDGE('',*,*,#3952,.F.);
#5155=ORIENTED_EDGE('',*,*,#3955,.F.);
#5156=ORIENTED_EDGE('',*,*,#3958,.F.);
#5157=ORIENTED_EDGE('',*,*,#3961,.F.);
#5158=ORIENTED_EDGE('',*,*,#3964,.F.);
#5159=ORIENTED_EDGE('',*,*,#3965,.F.);
#5160=ORIENTED_EDGE('',*,*,#3966,.F.);
#5161=ORIENTED_EDGE('',*,*,#3967,.T.);
#5162=ORIENTED_EDGE('',*,*,#3965,.T.);
#5163=ORIENTED_EDGE('',*,*,#3967,.F.);
#5164=ORIENTED_EDGE('',*,*,#3968,.F.);
#5165=ORIENTED_EDGE('',*,*,#3969,.T.);
#5166=ORIENTED_EDGE('',*,*,#3966,.T.);
#5167=ORIENTED_EDGE('',*,*,#3969,.F.);
#5168=ORIENTED_EDGE('',*,*,#3970,.F.);
#5169=ORIENTED_EDGE('',*,*,#3971,.T.);
#5170=ORIENTED_EDGE('',*,*,#3968,.T.);
#5171=ORIENTED_EDGE('',*,*,#3971,.F.);
#5172=ORIENTED_EDGE('',*,*,#3970,.T.);
#5173=ORIENTED_EDGE('',*,*,#3972,.F.);
#5174=ORIENTED_EDGE('',*,*,#3973,.F.);
#5175=ORIENTED_EDGE('',*,*,#3974,.T.);
#5176=ORIENTED_EDGE('',*,*,#3972,.T.);
#5177=ORIENTED_EDGE('',*,*,#3974,.F.);
#5178=ORIENTED_EDGE('',*,*,#3964,.T.);
#5179=ORIENTED_EDGE('',*,*,#3975,.T.);
#5180=ORIENTED_EDGE('',*,*,#3973,.T.);
#5181=ORIENTED_EDGE('',*,*,#3975,.F.);
#5934=CYLINDRICAL_SURFACE('',#7004,0.425);
#5935=CYLINDRICAL_SURFACE('',#7012,0.24505);
#6145=ADVANCED_FACE('',(#1082),#800,.F.);
#6146=ADVANCED_FACE('',(#1083),#801,.F.);
#6147=ADVANCED_FACE('',(#1084),#802,.F.);
#6148=ADVANCED_FACE('',(#1085),#803,.F.);
#6149=ADVANCED_FACE('',(#1086),#804,.F.);
#6150=ADVANCED_FACE('',(#1087),#805,.F.);
#6151=ADVANCED_FACE('',(#1088),#806,.F.);
#6152=ADVANCED_FACE('',(#1089),#807,.F.);
#6153=ADVANCED_FACE('',(#1090),#808,.F.);
#6154=ADVANCED_FACE('',(#1091),#809,.T.);
#6155=ADVANCED_FACE('',(#1092),#393,.T.);
#6156=ADVANCED_FACE('',(#1093),#5934,.T.);
#6157=ADVANCED_FACE('',(#1094),#394,.T.);
#6158=ADVANCED_FACE('',(#1095,#613),#810,.T.);
#6159=ADVANCED_FACE('',(#1096),#395,.T.);
#6160=ADVANCED_FACE('',(#1097),#5935,.T.);
#6341=CLOSED_SHELL('',(#6145,#6146,#6147,#6148,#6149,#6150,#6151,#6152));
#6342=CLOSED_SHELL('',(#6153,#6154,#6155,#6156,#6157,#6158,#6159,#6160));
#6989=AXIS2_PLACEMENT_3D('',#10078,#8227,#8228);
#6990=AXIS2_PLACEMENT_3D('',#10079,#8229,#8230);
#6991=AXIS2_PLACEMENT_3D('',#10088,#8235,#8236);
#6992=AXIS2_PLACEMENT_3D('',#10094,#8240,#8241);
#6993=AXIS2_PLACEMENT_3D('',#10100,#8245,#8246);
#6994=AXIS2_PLACEMENT_3D('',#10106,#8250,#8251);
#6995=AXIS2_PLACEMENT_3D('',#10112,#8255,#8256);
#6996=AXIS2_PLACEMENT_3D('',#10115,#8259,#8260);
#6997=AXIS2_PLACEMENT_3D('',#10116,#8261,#8262);
#6998=AXIS2_PLACEMENT_3D('',#10117,#8263,#8264);
#6999=AXIS2_PLACEMENT_3D('',#10119,#8265,#8266);
#7000=AXIS2_PLACEMENT_3D('',#10120,#8267,#8268);
#7001=AXIS2_PLACEMENT_3D('',#10122,#8269,#8270);
#7002=AXIS2_PLACEMENT_3D('',#10123,#8271,#8272);
#7003=AXIS2_PLACEMENT_3D('',#10125,#8273,#8274);
#7004=AXIS2_PLACEMENT_3D('',#10127,#8276,#8277);
#7005=AXIS2_PLACEMENT_3D('',#10129,#8278,#8279);
#7006=AXIS2_PLACEMENT_3D('',#10131,#8281,#8282);
#7007=AXIS2_PLACEMENT_3D('',#10133,#8283,#8284);
#7008=AXIS2_PLACEMENT_3D('',#10135,#8286,#8287);
#7009=AXIS2_PLACEMENT_3D('',#10137,#8288,#8289);
#7010=AXIS2_PLACEMENT_3D('',#10138,#8290,#8291);
#7011=AXIS2_PLACEMENT_3D('',#10140,#8292,#8293);
#7012=AXIS2_PLACEMENT_3D('',#10142,#8295,#8296);
#8227=DIRECTION('axis',(0.,0.,1.));
#8228=DIRECTION('refdir',(1.,0.,0.));
#8229=DIRECTION('center_axis',(0.866025403784439,0.,-0.5));
#8230=DIRECTION('ref_axis',(0.5,0.,0.866025403784439));
#8231=DIRECTION('',(-0.5,0.,-0.866025403784439));
#8232=DIRECTION('',(0.,-1.,0.));
#8233=DIRECTION('',(0.5,0.,0.866025403784439));
#8234=DIRECTION('',(0.,-1.,0.));
#8235=DIRECTION('center_axis',(1.20185167898973E-16,0.,-1.));
#8236=DIRECTION('ref_axis',(1.,0.,1.20185167898973E-16));
#8237=DIRECTION('',(-1.,0.,-1.20185167898973E-16));
#8238=DIRECTION('',(0.,-1.,0.));
#8239=DIRECTION('',(1.,0.,1.20185167898973E-16));
#8240=DIRECTION('center_axis',(-0.866025403784439,0.,-0.5));
#8241=DIRECTION('ref_axis',(0.5,0.,-0.866025403784439));
#8242=DIRECTION('',(-0.5,0.,0.866025403784439));
#8243=DIRECTION('',(0.,-1.,0.));
#8244=DIRECTION('',(0.5,0.,-0.866025403784439));
#8245=DIRECTION('center_axis',(-0.866025403784439,0.,0.5));
#8246=DIRECTION('ref_axis',(-0.5,0.,-0.866025403784439));
#8247=DIRECTION('',(0.5,0.,0.866025403784439));
#8248=DIRECTION('',(0.,-1.,0.));
#8249=DIRECTION('',(-0.5,0.,-0.866025403784439));
#8250=DIRECTION('center_axis',(-2.40370335797945E-16,0.,1.));
#8251=DIRECTION('ref_axis',(-1.,0.,-2.40370335797945E-16));
#8252=DIRECTION('',(1.,0.,2.40370335797945E-16));
#8253=DIRECTION('',(0.,-1.,0.));
#8254=DIRECTION('',(-1.,0.,-2.40370335797945E-16));
#8255=DIRECTION('center_axis',(0.866025403784439,0.,0.5));
#8256=DIRECTION('ref_axis',(-0.5,0.,0.866025403784439));
#8257=DIRECTION('',(0.5,0.,-0.866025403784439));
#8258=DIRECTION('',(-0.5,0.,0.866025403784439));
#8259=DIRECTION('center_axis',(0.,1.,0.));
#8260=DIRECTION('ref_axis',(1.,0.,0.));
#8261=DIRECTION('center_axis',(0.,-1.,0.));
#8262=DIRECTION('ref_axis',(0.,0.,-1.));
#8263=DIRECTION('center_axis',(0.,1.,0.));
#8264=DIRECTION('ref_axis',(1.,0.,0.));
#8265=DIRECTION('center_axis',(0.,1.,0.));
#8266=DIRECTION('ref_axis',(1.,0.,0.));
#8267=DIRECTION('center_axis',(0.,1.,0.));
#8268=DIRECTION('ref_axis',(0.,0.,1.));
#8269=DIRECTION('center_axis',(0.,-1.,0.));
#8270=DIRECTION('ref_axis',(1.,0.,0.));
#8271=DIRECTION('center_axis',(0.,-1.,0.));
#8272=DIRECTION('ref_axis',(1.,0.,0.));
#8273=DIRECTION('center_axis',(0.,-1.,0.));
#8274=DIRECTION('ref_axis',(1.,0.,0.));
#8275=DIRECTION('',(0.707106781186548,0.707106781186547,8.65956056235493E-17));
#8276=DIRECTION('center_axis',(0.,-1.,0.));
#8277=DIRECTION('ref_axis',(1.,0.,0.));
#8278=DIRECTION('center_axis',(0.,-1.,0.));
#8279=DIRECTION('ref_axis',(1.,0.,0.));
#8280=DIRECTION('',(0.,1.,0.));
#8281=DIRECTION('center_axis',(0.,1.,0.));
#8282=DIRECTION('ref_axis',(1.,0.,0.));
#8283=DIRECTION('center_axis',(0.,-1.,0.));
#8284=DIRECTION('ref_axis',(1.,0.,0.));
#8285=DIRECTION('',(-0.707106781186547,0.707106781186548,-8.65956056235493E-17));
#8286=DIRECTION('center_axis',(0.,-1.,0.));
#8287=DIRECTION('ref_axis',(0.,0.,-1.));
#8288=DIRECTION('center_axis',(0.,-1.,0.));
#8289=DIRECTION('ref_axis',(1.,0.,0.));
#8290=DIRECTION('center_axis',(0.,1.,0.));
#8291=DIRECTION('ref_axis',(1.,0.,0.));
#8292=DIRECTION('center_axis',(0.,1.,0.));
#8293=DIRECTION('ref_axis',(1.,0.,0.));
#8294=DIRECTION('',(-0.447213595499958,0.894427190999916,-5.47678698264203E-17));
#8295=DIRECTION('center_axis',(0.,-1.,0.));
#8296=DIRECTION('ref_axis',(1.,0.,0.));
#8297=DIRECTION('',(0.,1.,0.));
#10078=CARTESIAN_POINT('',(0.,0.,0.));
#10079=CARTESIAN_POINT('Origin',(0.115470053837925,-0.5,-0.2));
#10080=CARTESIAN_POINT('',(0.23094010767585,-0.5,0.));
#10081=CARTESIAN_POINT('',(0.115470053837925,-0.5,-0.2));
#10082=CARTESIAN_POINT('',(0.23094010767585,-0.5,0.));
#10083=CARTESIAN_POINT('',(0.115470053837925,-0.8,-0.2));
#10084=CARTESIAN_POINT('',(0.115470053837925,-0.5,-0.2));
#10085=CARTESIAN_POINT('',(0.23094010767585,-0.8,0.));
#10086=CARTESIAN_POINT('',(0.23094010767585,-0.8,0.));
#10087=CARTESIAN_POINT('',(0.23094010767585,-0.5,0.));
#10088=CARTESIAN_POINT('Origin',(-0.115470053837925,-0.5,-0.2));
#10089=CARTESIAN_POINT('',(-0.115470053837925,-0.5,-0.2));
#10090=CARTESIAN_POINT('',(0.115470053837925,-0.5,-0.2));
#10091=CARTESIAN_POINT('',(-0.115470053837925,-0.8,-0.2));
#10092=CARTESIAN_POINT('',(-0.115470053837925,-0.5,-0.2));
#10093=CARTESIAN_POINT('',(0.115470053837925,-0.8,-0.2));
#10094=CARTESIAN_POINT('Origin',(-0.23094010767585,-0.5,-2.77555756156289E-17));
#10095=CARTESIAN_POINT('',(-0.23094010767585,-0.5,-2.82820063659975E-17));
#10096=CARTESIAN_POINT('',(-0.115470053837925,-0.5,-0.2));
#10097=CARTESIAN_POINT('',(-0.23094010767585,-0.8,-2.77555756156289E-17));
#10098=CARTESIAN_POINT('',(-0.23094010767585,-0.5,-2.82820063659975E-17));
#10099=CARTESIAN_POINT('',(-0.115470053837925,-0.8,-0.2));
#10100=CARTESIAN_POINT('Origin',(-0.115470053837925,-0.5,0.2));
#10101=CARTESIAN_POINT('',(-0.115470053837925,-0.5,0.2));
#10102=CARTESIAN_POINT('',(-0.23094010767585,-0.5,-2.82820063659975E-17));
#10103=CARTESIAN_POINT('',(-0.115470053837925,-0.8,0.2));
#10104=CARTESIAN_POINT('',(-0.115470053837925,-0.5,0.2));
#10105=CARTESIAN_POINT('',(-0.23094010767585,-0.8,-2.82820063659975E-17));
#10106=CARTESIAN_POINT('Origin',(0.115470053837925,-0.5,0.2));
#10107=CARTESIAN_POINT('',(0.115470053837925,-0.5,0.2));
#10108=CARTESIAN_POINT('',(-0.115470053837925,-0.5,0.2));
#10109=CARTESIAN_POINT('',(0.115470053837925,-0.8,0.2));
#10110=CARTESIAN_POINT('',(0.115470053837925,-0.5,0.2));
#10111=CARTESIAN_POINT('',(-0.115470053837925,-0.8,0.2));
#10112=CARTESIAN_POINT('Origin',(0.23094010767585,-0.5,0.));
#10113=CARTESIAN_POINT('',(0.115470053837925,-0.5,0.2));
#10114=CARTESIAN_POINT('',(0.115470053837925,-0.8,0.2));
#10115=CARTESIAN_POINT('Origin',(0.,-0.5,0.));
#10116=CARTESIAN_POINT('Origin',(0.,-0.8,0.));
#10117=CARTESIAN_POINT('Origin',(0.,-1.7,0.));
#10118=CARTESIAN_POINT('',(-0.24505,-1.7,3.00099698131059E-17));
#10119=CARTESIAN_POINT('Origin',(0.,-1.7,0.));
#10120=CARTESIAN_POINT('Origin',(0.375,0.5,0.));
#10121=CARTESIAN_POINT('',(-0.375,0.5,-4.59242549680257E-17));
#10122=CARTESIAN_POINT('Origin',(0.,0.5,0.));
#10123=CARTESIAN_POINT('Origin',(0.,0.475,0.));
#10124=CARTESIAN_POINT('',(-0.425,0.45,-5.20474889637625E-17));
#10125=CARTESIAN_POINT('Origin',(0.,0.45,0.));
#10126=CARTESIAN_POINT('',(-0.4,0.475,-4.89858719658941E-17));
#10127=CARTESIAN_POINT('Origin',(0.,0.24,0.));
#10128=CARTESIAN_POINT('',(-0.425,0.0299999999999998,-5.20474889637625E-17));
#10129=CARTESIAN_POINT('Origin',(0.,0.0299999999999998,0.));
#10130=CARTESIAN_POINT('',(-0.425,0.24,-5.20474889637625E-17));
#10131=CARTESIAN_POINT('Origin',(0.,0.0150000000000001,0.));
#10132=CARTESIAN_POINT('',(-0.395,4.85722573273506E-17,-4.83735485663204E-17));
#10133=CARTESIAN_POINT('Origin',(0.,0.,0.));
#10134=CARTESIAN_POINT('',(-0.41,0.0150000000000001,-5.02105187650415E-17));
#10135=CARTESIAN_POINT('Origin',(0.27,0.,0.));
#10136=CARTESIAN_POINT('',(-0.27,0.,-3.30654635769785E-17));
#10137=CARTESIAN_POINT('Origin',(0.,0.,0.));
#10138=CARTESIAN_POINT('Origin',(0.,-0.02,0.));
#10139=CARTESIAN_POINT('',(-0.24505,-0.0498999999999999,3.00099698131059E-17));
#10140=CARTESIAN_POINT('Origin',(0.,-0.0498999999999999,0.));
#10141=CARTESIAN_POINT('',(-0.26,-0.02,-3.18408167778312E-17));
#10142=CARTESIAN_POINT('Origin',(0.,-0.995,0.));
#10143=CARTESIAN_POINT('',(-0.24505,-0.995,-3.00099698131059E-17));
#11505=UNCERTAINTY_MEASURE_WITH_UNIT(LENGTH_MEASURE(0.001),#11560,
'DISTANCE_ACCURACY_VALUE',
'Maximum model space distance between geometric entities at asserted c
onnectivities');
#11522=UNCERTAINTY_MEASURE_WITH_UNIT(LENGTH_MEASURE(0.001),#11560,
'DISTANCE_ACCURACY_VALUE',
'Maximum model space distance between geometric entities at asserted c
onnectivities');
#11542=(
GEOMETRIC_REPRESENTATION_CONTEXT(3)
GLOBAL_UNCERTAINTY_ASSIGNED_CONTEXT((#11505))
GLOBAL_UNIT_ASSIGNED_CONTEXT((#11560,#11562,#11563))
REPRESENTATION_CONTEXT('','3D')
);
#11559=(
GEOMETRIC_REPRESENTATION_CONTEXT(3)
GLOBAL_UNCERTAINTY_ASSIGNED_CONTEXT((#11522))
GLOBAL_UNIT_ASSIGNED_CONTEXT((#11560,#11562,#11563))
REPRESENTATION_CONTEXT('','3D')
);
#11560=(
LENGTH_UNIT()
NAMED_UNIT(*)
SI_UNIT(.CENTI.,.METRE.)
);
#11562=(
NAMED_UNIT(*)
PLANE_ANGLE_UNIT()
SI_UNIT($,.RADIAN.)
);
#11563=(
NAMED_UNIT(*)
SI_UNIT($,.STERADIAN.)
SOLID_ANGLE_UNIT()
);
#11583=SHAPE_DEFINITION_REPRESENTATION(#11619,#11740);
#11619=PRODUCT_DEFINITION_SHAPE('',$,#11777);
#11740=SHAPE_REPRESENTATION('',(#6989),#11542);
#11757=PRODUCT_DEFINITION_CONTEXT('part definition',#11867,'design');
#11777=PRODUCT_DEFINITION('M5x17 screw','M5x17 screw',#11813,#11757);
#11813=PRODUCT_DEFINITION_FORMATION('',$,#11888);
#11867=APPLICATION_CONTEXT(
'Core Data for Automotive Mechanical Design Process');
#11868=PRODUCT_CONTEXT('part definition',#11867,'mechanical');
#11888=PRODUCT('M5x17 screw','M5x17 screw','M5x17 screw',(#11868));
#11968=COLOUR_RGB('Black',0.12,0.14,0.17);
#11969=FILL_AREA_STYLE_COLOUR('',#11968);
#11970=FILL_AREA_STYLE('',(#11969));
#11971=SURFACE_STYLE_FILL_AREA(#11970);
#11972=SURFACE_SIDE_STYLE('',(#11971));
#11973=SURFACE_STYLE_USAGE(.BOTH.,#11972);
#11974=PRESENTATION_STYLE_ASSIGNMENT((#11973));
ENDSEC;
END-ISO-10303-21;
